ISO-10303-21;
HEADER;
/* Generated by software containing ST-Developer
 * from STEP Tools, Inc. (www.steptools.com) 
 */

FILE_DESCRIPTION(
/* description */ ('Shaft runout checking stand'),
/* implementation_level */ '2;1');

FILE_NAME(
/* name */ 'Inner race spacer (4).step',
/* time_stamp */ '2026-11-02T21:12:33-08:00',
/* author */ (''),
/* organization */ (''),
/* preprocessor_version */ 'ST-DEVELOPER v20.2',
/* originating_system */ 'Autodesk Translation Framework v15.17.0.0',
/* authorisation */ '');

FILE_SCHEMA (('AUTOMOTIVE_DESIGN { 1 0 10303 214 3 1 1 }'));
ENDSEC;

DATA;
#10=MECHANICAL_DESIGN_GEOMETRIC_PRESENTATION_REPRESENTATION('',(#496),#11748);
#410=SHAPE_REPRESENTATION_RELATIONSHIP('SRR','None',#11959,#453);
#453=ADVANCED_BREP_SHAPE_REPRESENTATION('',(#544),#11735);
#496=STYLED_ITEM('',(#12170),#544);
#544=MANIFOLD_SOLID_BREP('Body1',#6242);
#656=FACE_BOUND('',#1801,.T.);
#657=FACE_BOUND('',#1803,.T.);
#848=CIRCLE('',#7246,0.505);
#849=CIRCLE('',#7247,0.505);
#850=CIRCLE('',#7249,0.7);
#851=CIRCLE('',#7250,0.7);
#1017=CYLINDRICAL_SURFACE('',#7245,0.505);
#1018=CYLINDRICAL_SURFACE('',#7248,0.7);
#1336=FACE_OUTER_BOUND('',#1798,.T.);
#1337=FACE_OUTER_BOUND('',#1799,.T.);
#1338=FACE_OUTER_BOUND('',#1800,.T.);
#1339=FACE_OUTER_BOUND('',#1802,.T.);
#1798=EDGE_LOOP('',(#5338,#5339,#5340,#5341));
#1799=EDGE_LOOP('',(#5342,#5343,#5344,#5345));
#1800=EDGE_LOOP('',(#5346));
#1801=EDGE_LOOP('',(#5347));
#1802=EDGE_LOOP('',(#5348));
#1803=EDGE_LOOP('',(#5349));
#2327=LINE('',#10929,#2794);
#2328=LINE('',#10935,#2795);
#2794=VECTOR('',#8960,0.505);
#2795=VECTOR('',#8967,0.7);
#3232=VERTEX_POINT('',#10926);
#3233=VERTEX_POINT('',#10928);
#3234=VERTEX_POINT('',#10932);
#3235=VERTEX_POINT('',#10934);
#3955=EDGE_CURVE('',#3232,#3232,#848,.T.);
#3956=EDGE_CURVE('',#3232,#3233,#2327,.T.);
#3957=EDGE_CURVE('',#3233,#3233,#849,.T.);
#3958=EDGE_CURVE('',#3234,#3234,#850,.T.);
#3959=EDGE_CURVE('',#3234,#3235,#2328,.T.);
#3960=EDGE_CURVE('',#3235,#3235,#851,.T.);
#5338=ORIENTED_EDGE('',*,*,#3955,.F.);
#5339=ORIENTED_EDGE('',*,*,#3956,.T.);
#5340=ORIENTED_EDGE('',*,*,#3957,.T.);
#5341=ORIENTED_EDGE('',*,*,#3956,.F.);
#5342=ORIENTED_EDGE('',*,*,#3958,.F.);
#5343=ORIENTED_EDGE('',*,*,#3959,.T.);
#5344=ORIENTED_EDGE('',*,*,#3960,.T.);
#5345=ORIENTED_EDGE('',*,*,#3959,.F.);
#5346=ORIENTED_EDGE('',*,*,#3958,.T.);
#5347=ORIENTED_EDGE('',*,*,#3955,.T.);
#5348=ORIENTED_EDGE('',*,*,#3960,.F.);
#5349=ORIENTED_EDGE('',*,*,#3957,.F.);
#5811=PLANE('',#7251);
#5812=PLANE('',#7252);
#6136=ADVANCED_FACE('',(#1336),#1017,.F.);
#6137=ADVANCED_FACE('',(#1337),#1018,.T.);
#6138=ADVANCED_FACE('',(#1338,#656),#5811,.T.);
#6139=ADVANCED_FACE('',(#1339,#657),#5812,.F.);
#6242=CLOSED_SHELL('',(#6136,#6137,#6138,#6139));
#7244=AXIS2_PLACEMENT_3D('',#10924,#8954,#8955);
#7245=AXIS2_PLACEMENT_3D('',#10925,#8956,#8957);
#7246=AXIS2_PLACEMENT_3D('',#10927,#8958,#8959);
#7247=AXIS2_PLACEMENT_3D('',#10930,#8961,#8962);
#7248=AXIS2_PLACEMENT_3D('',#10931,#8963,#8964);
#7249=AXIS2_PLACEMENT_3D('',#10933,#8965,#8966);
#7250=AXIS2_PLACEMENT_3D('',#10936,#8968,#8969);
#7251=AXIS2_PLACEMENT_3D('',#10937,#8970,#8971);
#7252=AXIS2_PLACEMENT_3D('',#10938,#8972,#8973);
#8954=DIRECTION('axis',(0.,0.,1.));
#8955=DIRECTION('refdir',(1.,0.,0.));
#8956=DIRECTION('center_axis',(0.,1.,0.));
#8957=DIRECTION('ref_axis',(1.,0.,0.));
#8958=DIRECTION('center_axis',(0.,-1.,0.));
#8959=DIRECTION('ref_axis',(1.,0.,0.));
#8960=DIRECTION('',(0.,-1.,0.));
#8961=DIRECTION('center_axis',(0.,-1.,0.));
#8962=DIRECTION('ref_axis',(1.,0.,0.));
#8963=DIRECTION('center_axis',(0.,1.,0.));
#8964=DIRECTION('ref_axis',(1.,0.,0.));
#8965=DIRECTION('center_axis',(0.,1.,0.));
#8966=DIRECTION('ref_axis',(1.,0.,0.));
#8967=DIRECTION('',(0.,-1.,0.));
#8968=DIRECTION('center_axis',(0.,1.,0.));
#8969=DIRECTION('ref_axis',(1.,0.,0.));
#8970=DIRECTION('center_axis',(0.,1.,0.));
#8971=DIRECTION('ref_axis',(1.,0.,0.));
#8972=DIRECTION('center_axis',(0.,1.,0.));
#8973=DIRECTION('ref_axis',(1.,0.,0.));
#10924=CARTESIAN_POINT('',(0.,0.,0.));
#10925=CARTESIAN_POINT('Origin',(-2.,9.2,5.));
#10926=CARTESIAN_POINT('',(-2.505,9.55,5.));
#10927=CARTESIAN_POINT('Origin',(-2.,9.55,5.));
#10928=CARTESIAN_POINT('',(-2.505,9.2,5.));
#10929=CARTESIAN_POINT('',(-2.505,9.2,5.));
#10930=CARTESIAN_POINT('Origin',(-2.,9.2,5.));
#10931=CARTESIAN_POINT('Origin',(-2.,9.2,5.));
#10932=CARTESIAN_POINT('',(-2.7,9.55,5.));
#10933=CARTESIAN_POINT('Origin',(-2.,9.55,5.));
#10934=CARTESIAN_POINT('',(-2.7,9.2,5.));
#10935=CARTESIAN_POINT('',(-2.7,9.2,5.));
#10936=CARTESIAN_POINT('Origin',(-2.,9.2,5.));
#10937=CARTESIAN_POINT('Origin',(-2.,9.55,5.));
#10938=CARTESIAN_POINT('Origin',(-2.,9.2,5.));
#11686=UNCERTAINTY_MEASURE_WITH_UNIT(LENGTH_MEASURE(0.001),#11749,
'DISTANCE_ACCURACY_VALUE',
'Maximum model space distance between geometric entities at asserted c
onnectivities');
#11699=UNCERTAINTY_MEASURE_WITH_UNIT(LENGTH_MEASURE(0.001),#11749,
'DISTANCE_ACCURACY_VALUE',
'Maximum model space distance between geometric entities at asserted c
onnectivities');
#11735=(
GEOMETRIC_REPRESENTATION_CONTEXT(3)
GLOBAL_UNCERTAINTY_ASSIGNED_CONTEXT((#11686))
GLOBAL_UNIT_ASSIGNED_CONTEXT((#11749,#11751,#11752))
REPRESENTATION_CONTEXT('','3D')
);
#11748=(
GEOMETRIC_REPRESENTATION_CONTEXT(3)
GLOBAL_UNCERTAINTY_ASSIGNED_CONTEXT((#11699))
GLOBAL_UNIT_ASSIGNED_CONTEXT((#11749,#11751,#11752))
REPRESENTATION_CONTEXT('','3D')
);
#11749=(
LENGTH_UNIT()
NAMED_UNIT(*)
SI_UNIT(.CENTI.,.METRE.)
);
#11751=(
NAMED_UNIT(*)
PLANE_ANGLE_UNIT()
SI_UNIT($,.RADIAN.)
);
#11752=(
NAMED_UNIT(*)
SI_UNIT($,.STERADIAN.)
SOLID_ANGLE_UNIT()
);
#11788=SHAPE_DEFINITION_REPRESENTATION(#11836,#11959);
#11836=PRODUCT_DEFINITION_SHAPE('',$,#12008);
#11959=SHAPE_REPRESENTATION('',(#7244),#11735);
#11972=PRODUCT_DEFINITION_CONTEXT('part definition',#12118,'design');
#12008=PRODUCT_DEFINITION('Inner race spacer_7','Inner race spacer (4)',
#12056,#11972);
#12056=PRODUCT_DEFINITION_FORMATION('',$,#12155);
#12118=APPLICATION_CONTEXT(
'Core Data for Automotive Mechanical Design Process');
#12119=PRODUCT_CONTEXT('part definition',#12118,'mechanical');
#12155=PRODUCT('Inner race spacer_7','Inner race spacer (4)',
'Inner race spacer',(#12119));
#12170=PRESENTATION_STYLE_ASSIGNMENT((#12175));
#12175=SURFACE_STYLE_USAGE(.BOTH.,#12180);
#12180=SURFACE_SIDE_STYLE('',(#12185));
#12185=SURFACE_STYLE_FILL_AREA(#12190);
#12190=FILL_AREA_STYLE('CAD Library Painted - Steel gray',(#12195));
#12195=FILL_AREA_STYLE_COLOUR('CAD Library Painted - Steel gray',#12200);
#12200=COLOUR_RGB('CAD Library Painted - Steel gray',0.592156862745098,
0.631372549019608,0.67843137254902);
ENDSEC;
END-ISO-10303-21;
